ISO-10303-21;
HEADER;
/* Generated by software containing ST-Developer
 * from STEP Tools, Inc. (www.steptools.com) 
 */

FILE_DESCRIPTION(
/* description */ ('Belt-driven linear axis on 2020 extrusion'),
/* implementation_level */ '2;1');

FILE_NAME(
/* name */ 'Input M3 set screw (3).step',
/* time_stamp */ '2026-10-28T03:26:09-07:00',
/* author */ (''),
/* organization */ (''),
/* preprocessor_version */ 'ST-DEVELOPER v20.2',
/* originating_system */ 'Autodesk Translation Framework v15.17.0.0',
/* authorisation */ '');

FILE_SCHEMA (('AUTOMOTIVE_DESIGN { 1 0 10303 214 3 1 1 }'));
ENDSEC;

DATA;
#10=MECHANICAL_DESIGN_GEOMETRIC_PRESENTATION_REPRESENTATION('',(#653),#20096);
#551=SHAPE_REPRESENTATION_RELATIONSHIP('SRR','None',#20350,#597);
#597=ADVANCED_BREP_SHAPE_REPRESENTATION('',(#708),#20081);
#653=STYLED_ITEM('',(#20657),#708);
#708=MANIFOLD_SOLID_BREP('Body1',#10967);
#1140=PLANE('',#12309);
#1141=PLANE('',#12310);
#1673=FACE_OUTER_BOUND('',#2426,.T.);
#1674=FACE_OUTER_BOUND('',#2427,.T.);
#1675=FACE_OUTER_BOUND('',#2428,.T.);
#2426=EDGE_LOOP('',(#9115,#9116,#9117,#9118));
#2427=EDGE_LOOP('',(#9119));
#2428=EDGE_LOOP('',(#9120));
#3229=LINE('',#18601,#4086);
#4086=VECTOR('',#14985,0.149999999999999);
#4726=CIRCLE('',#12307,0.149999999999999);
#4727=CIRCLE('',#12308,0.149999999999999);
#5521=VERTEX_POINT('',#18598);
#5522=VERTEX_POINT('',#18600);
#6772=EDGE_CURVE('',#5521,#5521,#4726,.T.);
#6773=EDGE_CURVE('',#5521,#5522,#3229,.T.);
#6774=EDGE_CURVE('',#5522,#5522,#4727,.T.);
#9115=ORIENTED_EDGE('',*,*,#6772,.F.);
#9116=ORIENTED_EDGE('',*,*,#6773,.T.);
#9117=ORIENTED_EDGE('',*,*,#6774,.T.);
#9118=ORIENTED_EDGE('',*,*,#6773,.F.);
#9119=ORIENTED_EDGE('',*,*,#6772,.T.);
#9120=ORIENTED_EDGE('',*,*,#6774,.F.);
#10224=CYLINDRICAL_SURFACE('',#12306,0.149999999999999);
#10724=ADVANCED_FACE('',(#1673),#10224,.T.);
#10725=ADVANCED_FACE('',(#1674),#1140,.T.);
#10726=ADVANCED_FACE('',(#1675),#1141,.F.);
#10967=CLOSED_SHELL('',(#10724,#10725,#10726));
#12305=AXIS2_PLACEMENT_3D('',#18596,#14979,#14980);
#12306=AXIS2_PLACEMENT_3D('',#18597,#14981,#14982);
#12307=AXIS2_PLACEMENT_3D('',#18599,#14983,#14984);
#12308=AXIS2_PLACEMENT_3D('',#18602,#14986,#14987);
#12309=AXIS2_PLACEMENT_3D('',#18603,#14988,#14989);
#12310=AXIS2_PLACEMENT_3D('',#18604,#14990,#14991);
#14979=DIRECTION('axis',(0.,0.,1.));
#14980=DIRECTION('refdir',(1.,0.,0.));
#14981=DIRECTION('center_axis',(0.,0.,1.));
#14982=DIRECTION('ref_axis',(1.,0.,0.));
#14983=DIRECTION('center_axis',(0.,0.,1.));
#14984=DIRECTION('ref_axis',(1.,0.,0.));
#14985=DIRECTION('',(0.,0.,-1.));
#14986=DIRECTION('center_axis',(0.,0.,1.));
#14987=DIRECTION('ref_axis',(1.,0.,0.));
#14988=DIRECTION('center_axis',(0.,0.,1.));
#14989=DIRECTION('ref_axis',(1.,0.,0.));
#14990=DIRECTION('center_axis',(0.,0.,1.));
#14991=DIRECTION('ref_axis',(1.,0.,0.));
#18596=CARTESIAN_POINT('',(0.,0.,0.));
#18597=CARTESIAN_POINT('Origin',(32.,-3.95,7.4));
#18598=CARTESIAN_POINT('',(31.85,-3.95,7.65));
#18599=CARTESIAN_POINT('Origin',(32.,-3.95,7.65));
#18600=CARTESIAN_POINT('',(31.85,-3.95,7.4));
#18601=CARTESIAN_POINT('',(31.85,-3.95,7.4));
#18602=CARTESIAN_POINT('Origin',(32.,-3.95,7.4));
#18603=CARTESIAN_POINT('Origin',(32.,-3.95,7.65));
#18604=CARTESIAN_POINT('Origin',(32.,-3.95,7.4));
#20027=UNCERTAINTY_MEASURE_WITH_UNIT(LENGTH_MEASURE(0.001),#20097,
'DISTANCE_ACCURACY_VALUE',
'Maximum model space distance between geometric entities at asserted c
onnectivities');
#20042=UNCERTAINTY_MEASURE_WITH_UNIT(LENGTH_MEASURE(0.001),#20097,
'DISTANCE_ACCURACY_VALUE',
'Maximum model space distance between geometric entities at asserted c
onnectivities');
#20081=(
GEOMETRIC_REPRESENTATION_CONTEXT(3)
GLOBAL_UNCERTAINTY_ASSIGNED_CONTEXT((#20027))
GLOBAL_UNIT_ASSIGNED_CONTEXT((#20097,#20099,#20100))
REPRESENTATION_CONTEXT('','3D')
);
#20096=(
GEOMETRIC_REPRESENTATION_CONTEXT(3)
GLOBAL_UNCERTAINTY_ASSIGNED_CONTEXT((#20042))
GLOBAL_UNIT_ASSIGNED_CONTEXT((#20097,#20099,#20100))
REPRESENTATION_CONTEXT('','3D')
);
#20097=(
LENGTH_UNIT()
NAMED_UNIT(*)
SI_UNIT(.CENTI.,.METRE.)
);
#20099=(
NAMED_UNIT(*)
PLANE_ANGLE_UNIT()
SI_UNIT($,.RADIAN.)
);
#20100=(
NAMED_UNIT(*)
SI_UNIT($,.STERADIAN.)
SOLID_ANGLE_UNIT()
);
#20139=SHAPE_DEFINITION_REPRESENTATION(#20197,#20350);
#20197=PRODUCT_DEFINITION_SHAPE('',$,#20404);
#20350=SHAPE_REPRESENTATION('',(#12305),#20081);
#20365=PRODUCT_DEFINITION_CONTEXT('part definition',#20526,'design');
#20404=PRODUCT_DEFINITION('Input M3 set screw (3)',
'Input M3 set screw (3)',#20457,#20365);
#20457=PRODUCT_DEFINITION_FORMATION('',$,#20566);
#20526=APPLICATION_CONTEXT(
'Core Data for Automotive Mechanical Design Process');
#20527=PRODUCT_CONTEXT('part definition',#20526,'mechanical');
#20566=PRODUCT('Input M3 set screw (3)','Input M3 set screw (3)',
'Input M3 set screw (3)',(#20527));
#20651=COLOUR_RGB('Black',0.12,0.14,0.17);
#20652=FILL_AREA_STYLE_COLOUR('',#20651);
#20653=FILL_AREA_STYLE('',(#20652));
#20654=SURFACE_STYLE_FILL_AREA(#20653);
#20655=SURFACE_SIDE_STYLE('',(#20654));
#20656=SURFACE_STYLE_USAGE(.BOTH.,#20655);
#20657=PRESENTATION_STYLE_ASSIGNMENT((#20656));
ENDSEC;
END-ISO-10303-21;
